ISO-10303-21;
HEADER;
FILE_DESCRIPTION (('STEP AP214'),
    '1' );
FILE_NAME ('socket head cap screw_iso_ISO 4762 M4 x 30 - 20N.step',
    '2026-10-03T20:08:58',
    ( '' ),
    ( '' ),
    'SwSTEP 2.0',
    'SolidWorks 2026',
    '' );
FILE_SCHEMA (( 'AUTOMOTIVE_DESIGN' ));
ENDSEC;

DATA;
#4=CARTESIAN_POINT ( 'NONE',  ( 34.00000000000000000, 0.000000000000000000, -1.734723475976807094E-14 ) ) ;
#8=SHAPE_REPRESENTATION_RELATIONSHIP ( 'NONE' , 'NONE' ,  #10094, #6187 ) ;
#72=CARTESIAN_POINT ( 'NONE',  ( 2.000000000000001776, 1.773042676681341856, -3.469446951953614189E-15 ) ) ;
#106=CONICAL_SURFACE ( 'NONE', #7315, 1.535500000000000087, 1.047197551196590748 ) ;
#119=ORIENTED_EDGE ( 'NONE', *, *, #7545, .T. ) ;
#136=DIRECTION ( 'NONE',  ( 1.000000000000000000, 0.000000000000000000, 0.000000000000000000 ) ) ;
#138=PRODUCT_DEFINITION_FORMATION_WITH_SPECIFIED_SOURCE ( 'ANY', '', #5241, .NOT_KNOWN. ) ;
#141=ADVANCED_FACE ( 'NONE', ( #9022 ), #11990, .F. ) ;
#152=FACE_OUTER_BOUND ( 'NONE', #1535, .T. ) ;
#154=EDGE_CURVE ( 'NONE', #6728, #2957, #12005, .T. ) ;
#161=DIRECTION ( 'NONE',  ( 0.000000000000000000, 0.000000000000000000, 1.000000000000000000 ) ) ;
#193=( NAMED_UNIT ( * ) PLANE_ANGLE_UNIT ( ) SI_UNIT ( $, .RADIAN. ) );
#201=DIRECTION ( 'NONE',  ( 0.000000000000000000, 0.4999999999999989453, -0.8660254037844392627 ) ) ;
#208=CARTESIAN_POINT ( 'NONE',  ( 0.000000000000000000, 0.000000000000000000, 0.000000000000000000 ) ) ;
#212=CARTESIAN_POINT ( 'NONE',  ( 2.000000000000001776, -1.773042676681341856, 3.469446951953614189E-15 ) ) ;
#217=EDGE_CURVE ( 'NONE', #10195, #4167, #2330, .T. ) ;
#218=CARTESIAN_POINT ( 'NONE',  ( 2.000000000000001776, -0.8865213383406691516, 1.535500000000002085 ) ) ;
#233=DIRECTION ( 'NONE',  ( 0.000000000000000000, 0.8660254037844380415, -0.5000000000000012212 ) ) ;
#251=DIRECTION ( 'NONE',  ( -1.000000000000000000, -0.000000000000000000, -0.000000000000000000 ) ) ;
#255=( LENGTH_UNIT ( ) NAMED_UNIT ( * ) SI_UNIT ( .MILLI., .METRE. ) );
#283=CARTESIAN_POINT ( 'NONE',  ( 2.000000000000001776, 1.773042676681341856, -3.469446951953614189E-15 ) ) ;
#297=FACE_OUTER_BOUND ( 'NONE', #12054, .T. ) ;
#318=DIRECTION ( 'NONE',  ( 0.000000000000000000, -1.000000000000000000, 8.560894001270036306E-16 ) ) ;
#321=DIRECTION ( 'NONE',  ( 0.000000000000000000, -1.000000000000000000, 0.000000000000000000 ) ) ;
#354=AXIS2_PLACEMENT_3D ( 'NONE', #7776, #2780, #817 ) ;
#381=CARTESIAN_POINT ( 'NONE',  ( 34.00000000000000000, 2.210487472460973191E-16, -1.610000000000017417 ) ) ;
#393=ORIENTED_EDGE ( 'NONE', *, *, #2969, .F. ) ;
#446=DIRECTION ( 'NONE',  ( 0.000000000000000000, 0.000000000000000000, 1.000000000000000000 ) ) ;
#450=EDGE_CURVE ( 'NONE', #4892, #8146, #2866, .T. ) ;
#456=LINE ( 'NONE', #2532, #2255 ) ;
#473=ORIENTED_EDGE ( 'NONE', *, *, #1787, .F. ) ;
#481=EDGE_CURVE ( 'NONE', #1188, #12214, #2518, .T. ) ;
#562=VECTOR ( 'NONE', #12140, 999.9999999999998863 ) ;
#569=CARTESIAN_POINT ( 'NONE',  ( 0.000000000000000000, 0.000000000000000000, 3.299999999999999822 ) ) ;
#573=EDGE_LOOP ( 'NONE', ( #4853, #5435, #11535, #9853, #12243 ) ) ;
#602=ORIENTED_EDGE ( 'NONE', *, *, #3672, .F. ) ;
#607=CONICAL_SURFACE ( 'NONE', #3311, 1.610000000000000098, 0.7853981633974652654 ) ;
#610=VECTOR ( 'NONE', #8698, 1000.000000000000000 ) ;
#624=TOROIDAL_SURFACE ( 'NONE', #7821, 3.299999999999999822, 0.2000000000000000111 ) ;
#636=EDGE_LOOP ( 'NONE', ( #8469, #3542, #10384, #4361 ) ) ;
#660=ADVANCED_FACE ( 'NONE', ( #5603, #1675 ), #8249, .T. ) ;
#682=ORIENTED_EDGE ( 'NONE', *, *, #2205, .T. ) ;
#690=AXIS2_PLACEMENT_3D ( 'NONE', #10582, #5815, #11751 ) ;
#692=CARTESIAN_POINT ( 'NONE',  ( 33.61000000000001364, 2.449293598294697047E-16, -2.000000000000000888 ) ) ;
#694=UNCERTAINTY_MEASURE_WITH_UNIT (LENGTH_MEASURE( 1.000000000000000082E-05 ), #1092, 'distance_accuracy_value', 'NONE');
#696=EDGE_CURVE ( 'NONE', #7580, #4994, #1265, .T. ) ;
#769=ADVANCED_FACE ( 'NONE', ( #3739 ), #9034, .T. ) ;
#784=LINE ( 'NONE', #11558, #3995 ) ;
#787=CARTESIAN_POINT ( 'NONE',  ( 0.000000000000000000, 1.773042676681341856, -3.469446951953614189E-15 ) ) ;
#789=VECTOR ( 'NONE', #11946, 1000.000000000000114 ) ;
#817=DIRECTION ( 'NONE',  ( 0.000000000000000000, 0.000000000000000000, -1.000000000000000000 ) ) ;
#836=DIRECTION ( 'NONE',  ( 0.000000000000000000, 0.000000000000000000, -1.000000000000000000 ) ) ;
#852=EDGE_CURVE ( 'NONE', #1792, #10769, #12505, .T. ) ;
#860=LINE ( 'NONE', #9730, #6762 ) ;
#877=EDGE_CURVE ( 'NONE', #2957, #11940, #8218, .T. ) ;
#888=CARTESIAN_POINT ( 'NONE',  ( 0.000000000000000000, -0.8865213383406691516, 1.535500000000002085 ) ) ;
#899=DIRECTION ( 'NONE',  ( 1.000000000000000000, 0.000000000000000000, 0.000000000000000000 ) ) ;
#917=CARTESIAN_POINT ( 'NONE',  ( 4.000000000000003553, 2.694222958124189825E-16, 2.199999999999992184 ) ) ;
#919=ORIENTED_EDGE ( 'NONE', *, *, #10805, .F. ) ;
#961=DIRECTION ( 'NONE',  ( 0.000000000000000000, 0.000000000000000000, 1.000000000000000000 ) ) ;
#982=CARTESIAN_POINT ( 'NONE',  ( 2.000000000000091926, 0.8865213383406691516, -1.535500000000002085 ) ) ;
#1001=CARTESIAN_POINT ( 'NONE',  ( 0.1999999999999987899, 4.286263797015736595E-16, -3.500000000000017319 ) ) ;
#1018=ORIENTED_EDGE ( 'NONE', *, *, #12161, .F. ) ;
#1067=APPLICATION_CONTEXT ( 'automotive_design' ) ;
#1072=CIRCLE ( 'NONE', #4778, 3.500000000000000000 ) ;
#1091=LINE ( 'NONE', #8882, #6645 ) ;
#1092=( LENGTH_UNIT ( ) NAMED_UNIT ( * ) SI_UNIT ( .MILLI., .METRE. ) );
#1100=CARTESIAN_POINT ( 'NONE',  ( 2.000000000000001776, 0.8865213383406727043, 1.535499999999998755 ) ) ;
#1133=ORIENTED_EDGE ( 'NONE', *, *, #3535, .F. ) ;
#1134=DIRECTION ( 'NONE',  ( -1.000000000000000000, 0.000000000000000000, 0.000000000000000000 ) ) ;
#1145=EDGE_CURVE ( 'NONE', #1407, #11320, #6564, .T. ) ;
#1165=DIRECTION ( 'NONE',  ( 0.000000000000000000, 0.000000000000000000, -1.000000000000000000 ) ) ;
#1188=VERTEX_POINT ( 'NONE', #7564 ) ;
#1220=CARTESIAN_POINT ( 'NONE',  ( 0.000000000000000000, -1.773042676681341856, 3.469446951953614189E-15 ) ) ;
#1236=CARTESIAN_POINT ( 'NONE',  ( -31.74999999999995026, 2.449293598294707893E-16, -2.000000000000018208 ) ) ;
#1260=ORIENTED_EDGE ( 'NONE', *, *, #7203, .T. ) ;
#1262=EDGE_CURVE ( 'NONE', #1632, #10195, #8192, .T. ) ;
#1265=CIRCLE ( 'NONE', #10096, 3.500000000000000000 ) ;
#1277=ORIENTED_EDGE ( 'NONE', *, *, #10967, .F. ) ;
#1280=DIRECTION ( 'NONE',  ( -1.000000000000000000, 0.000000000000000000, 0.000000000000000000 ) ) ;
#1282=EDGE_CURVE ( 'NONE', #11062, #11320, #6003, .T. ) ;
#1285=EDGE_CURVE ( 'NONE', #8536, #5702, #860, .T. ) ;
#1292=AXIS2_PLACEMENT_3D ( 'NONE', #3598, #12546, #5457 ) ;
#1298=DIRECTION ( 'NONE',  ( 1.000000000000000000, 0.000000000000000000, 0.000000000000000000 ) ) ;
#1339=ADVANCED_FACE ( 'NONE', ( #6072 ), #10961, .T. ) ;
#1346=DIRECTION ( 'NONE',  ( 0.000000000000000000, 0.000000000000000000, 1.000000000000000000 ) ) ;
#1351=LINE ( 'NONE', #8252, #5877 ) ;
#1353=ADVANCED_FACE ( 'NONE', ( #4624 ), #6691, .T. ) ;
#1406=ORIENTED_EDGE ( 'NONE', *, *, #852, .F. ) ;
#1407=VERTEX_POINT ( 'NONE', #5459 ) ;
#1413=AXIS2_PLACEMENT_3D ( 'NONE', #283, #3270, #3142 ) ;
#1419=EDGE_LOOP ( 'NONE', ( #3925, #6074, #4357, #7931, #7137 ) ) ;
#1423=CIRCLE ( 'NONE', #9627, 0.2000000000000000944 ) ;
#1469=FACE_OUTER_BOUND ( 'NONE', #12351, .T. ) ;
#1475=DIRECTION ( 'NONE',  ( 0.000000000000000000, 0.000000000000000000, 1.000000000000000000 ) ) ;
#1505=VECTOR ( 'NONE', #12469, 1000.000000000000114 ) ;
#1535=EDGE_LOOP ( 'NONE', ( #8025, #1673, #2551, #10246 ) ) ;
#1538=DIRECTION ( 'NONE',  ( 1.000000000000000000, 0.000000000000000000, 0.000000000000000000 ) ) ;
#1556=EDGE_LOOP ( 'NONE', ( #9726, #8104, #3428, #4027, #5974 ) ) ;
#1569=ORIENTED_EDGE ( 'NONE', *, *, #8920, .T. ) ;
#1632=VERTEX_POINT ( 'NONE', #1001 ) ;
#1673=ORIENTED_EDGE ( 'NONE', *, *, #5824, .F. ) ;
#1675=FACE_OUTER_BOUND ( 'NONE', #12675, .T. ) ;
#1680=EDGE_LOOP ( 'NONE', ( #10061, #10515, #602, #1018 ) ) ;
#1710=EDGE_LOOP ( 'NONE', ( #11981, #7930, #10266 ) ) ;
#1743=AXIS2_PLACEMENT_3D ( 'NONE', #4385, #9515, #11278 ) ;
#1746=DIRECTION ( 'NONE',  ( 0.000000000000000000, 0.000000000000000000, 1.000000000000000000 ) ) ;
#1763=VERTEX_POINT ( 'NONE', #11768 ) ;
#1783=DIRECTION ( 'NONE',  ( -1.000000000000000000, 0.000000000000000000, 0.000000000000000000 ) ) ;
#1787=EDGE_CURVE ( 'NONE', #9004, #2431, #10718, .T. ) ;
#1792=VERTEX_POINT ( 'NONE', #7575 ) ;
#1794=CARTESIAN_POINT ( 'NONE',  ( 2.000000000000001776, 1.773042676681341856, -3.469446951953614189E-15 ) ) ;
#1821=AXIS2_PLACEMENT_3D ( 'NONE', #212, #8058, #5111 ) ;
#1824=CARTESIAN_POINT ( 'NONE',  ( 2.000000000000001776, -0.8865213383406691516, 1.535500000000002085 ) ) ;
#1826=CARTESIAN_POINT ( 'NONE',  ( 0.1999999999999987899, 4.041334437186265510E-16, -3.300000000000017142 ) ) ;
#1866=DIRECTION ( 'NONE',  ( 0.000000000000000000, 0.000000000000000000, -1.000000000000000000 ) ) ;
#1887=ORIENTED_EDGE ( 'NONE', *, *, #3389, .T. ) ;
#1923=DIRECTION ( 'NONE',  ( 0.000000000000000000, 0.000000000000000000, -1.000000000000000000 ) ) ;
#1934=CARTESIAN_POINT ( 'NONE',  ( 34.00000000000000000, 0.000000000000000000, -1.734723475976807094E-14 ) ) ;
#1949=ORIENTED_EDGE ( 'NONE', *, *, #11374, .T. ) ;
#1994=( NAMED_UNIT ( * ) SI_UNIT ( $, .STERADIAN. ) SOLID_ANGLE_UNIT ( ) );
#1999=EDGE_CURVE ( 'NONE', #5702, #5083, #6986, .T. ) ;
#2012=FACE_OUTER_BOUND ( 'NONE', #573, .T. ) ;
#2025=PRODUCT_CONTEXT ( 'NONE', #2397, 'mechanical' ) ;
#2038=ORIENTED_EDGE ( 'NONE', *, *, #10834, .F. ) ;
#2052=AXIS2_PLACEMENT_3D ( 'NONE', #6837, #899, #1866 ) ;
#2059=CARTESIAN_POINT ( 'NONE',  ( 9.714451465470119729E-14, -0.8865213383406727043, -1.535499999999998755 ) ) ;
#2064=PRESENTATION_STYLE_ASSIGNMENT (( #10877 ) ) ;
#2065=VECTOR ( 'NONE', #7917, 1000.000000000000227 ) ;
#2122=ORIENTED_EDGE ( 'NONE', *, *, #3535, .T. ) ;
#2205=EDGE_CURVE ( 'NONE', #4950, #5083, #2930, .T. ) ;
#2252=ORIENTED_EDGE ( 'NONE', *, *, #8762, .T. ) ;
#2255=VECTOR ( 'NONE', #5483, 999.9999999999998863 ) ;
#2272=FACE_OUTER_BOUND ( 'NONE', #4673, .T. ) ;
#2282=CARTESIAN_POINT ( 'NONE',  ( 4.200000000000001954, 0.000000000000000000, -1.734723475976807094E-14 ) ) ;
#2295=COLOUR_RGB ( '', 0.40784314, 0.44705882, 0.49803922) ;
#2303=DIRECTION ( 'NONE',  ( 0.000000000000000000, 0.000000000000000000, -1.000000000000000000 ) ) ;
#2306=CARTESIAN_POINT ( 'NONE',  ( 2.000000000000001776, 1.773042676681341856, -3.469446951953614189E-15 ) ) ;
#2313=CARTESIAN_POINT ( 'NONE',  ( 2.000000000000091926, 0.8865213383406691516, -1.535500000000002085 ) ) ;
#2316=ORIENTED_EDGE ( 'NONE', *, *, #7837, .T. ) ;
#2326=ORIENTED_EDGE ( 'NONE', *, *, #877, .T. ) ;
#2330=CIRCLE ( 'NONE', #2535, 3.299999999999999822 ) ;
#2344=EDGE_LOOP ( 'NONE', ( #12568, #3684 ) ) ;
#2359=EDGE_CURVE ( 'NONE', #1763, #10769, #4190, .T. ) ;
#2393=DIRECTION ( 'NONE',  ( 0.000000000000000000, 0.000000000000000000, -1.000000000000000000 ) ) ;
#2397=APPLICATION_CONTEXT ( 'automotive_design' ) ;
#2413=ADVANCED_FACE ( 'NONE', ( #4313 ), #12563, .F. ) ;
#2431=VERTEX_POINT ( 'NONE', #5279 ) ;
#2448=VECTOR ( 'NONE', #8754, 1000.000000000000000 ) ;
#2475=LINE ( 'NONE', #10373, #2849 ) ;
#2485=CARTESIAN_POINT ( 'NONE',  ( 0.000000000000000000, 4.163799117100989712E-16, -3.299999999999999822 ) ) ;
#2487=CARTESIAN_POINT ( 'NONE',  ( 2.000000000000001776, -1.329782007511007169, 0.7677500000000010427 ) ) ;
#2497=VERTEX_POINT ( 'NONE', #7348 ) ;
#2505=LINE ( 'NONE', #5642, #4180 ) ;
#2516=ADVANCED_FACE ( 'NONE', ( #2656 ), #624, .T. ) ;
#2518=CIRCLE ( 'NONE', #9077, 1.610000000000000098 ) ;
#2532=CARTESIAN_POINT ( 'NONE',  ( 0.000000000000000000, 1.773042676681341856, -3.469446951953614189E-15 ) ) ;
#2535=AXIS2_PLACEMENT_3D ( 'NONE', #11358, #4653, #11486 ) ;
#2551=ORIENTED_EDGE ( 'NONE', *, *, #12161, .T. ) ;
#2570=CIRCLE ( 'NONE', #4820, 3.500000000000000000 ) ;
#2571=SURFACE_STYLE_FILL_AREA ( #10337 ) ;
#2579=DIRECTION ( 'NONE',  ( 0.000000000000000000, 0.000000000000000000, 1.000000000000000000 ) ) ;
#2586=DIRECTION ( 'NONE',  ( -1.000000000000000000, 0.000000000000000000, 0.000000000000000000 ) ) ;
#2590=LINE ( 'NONE', #10428, #4849 ) ;
#2618=DIRECTION ( 'NONE',  ( 1.000000000000000000, -0.000000000000000000, -0.000000000000000000 ) ) ;
#2628=ORIENTED_EDGE ( 'NONE', *, *, #5794, .T. ) ;
#2656=FACE_OUTER_BOUND ( 'NONE', #1680, .T. ) ;
#2670=CIRCLE ( 'NONE', #9827, 2.000000000000000888 ) ;
#2686=AXIS2_PLACEMENT_3D ( 'NONE', #10737, #10986, #1923 ) ;
#2705=CIRCLE ( 'NONE', #7588, 1.610000000000000098 ) ;
#2740=PRODUCT_DEFINITION ( 'UNKNOWN', '', #138, #12305 ) ;
#2777=DIRECTION ( 'NONE',  ( 0.000000000000000000, 0.000000000000000000, 1.000000000000000000 ) ) ;
#2780=DIRECTION ( 'NONE',  ( 1.000000000000000000, 0.000000000000000000, 0.000000000000000000 ) ) ;
#2796=CARTESIAN_POINT ( 'NONE',  ( 2.000000000000001776, 1.880445160090761061E-16, -1.535500000000000087 ) ) ;
#2816=AXIS2_PLACEMENT_3D ( 'NONE', #3833, #7762, #12267 ) ;
#2819=LINE ( 'NONE', #1824, #8086 ) ;
#2849=VECTOR ( 'NONE', #4656, 1000.000000000000114 ) ;
#2863=CARTESIAN_POINT ( 'NONE',  ( 4.000000000000003553, 0.000000000000000000, -2.200000000000009504 ) ) ;
#2866=LINE ( 'NONE', #6847, #10925 ) ;
#2930=LINE ( 'NONE', #72, #2065 ) ;
#2957=VERTEX_POINT ( 'NONE', #12491 ) ;
#2969=EDGE_CURVE ( 'NONE', #4950, #11532, #3665, .T. ) ;
#2987=FILL_AREA_STYLE_COLOUR ( '', #2295 ) ;
#3025=EDGE_CURVE ( 'NONE', #4994, #7580, #2570, .T. ) ;
#3057=DIRECTION ( 'NONE',  ( 0.000000000000000000, 1.000000000000000000, -1.224646799147353207E-16 ) ) ;
#3107=DIRECTION ( 'NONE',  ( 0.000000000000000000, 0.4999999999999989453, -0.8660254037844392627 ) ) ;
#3119=( GEOMETRIC_REPRESENTATION_CONTEXT ( 3 ) GLOBAL_UNCERTAINTY_ASSIGNED_CONTEXT ( ( #694 ) ) GLOBAL_UNIT_ASSIGNED_CONTEXT ( ( #1092, #193, #1994 ) ) REPRESENTATION_CONTEXT ( 'NONE', 'WORKASPACE' ) );
#3140=EDGE_CURVE ( 'NONE', #11532, #10836, #10744, .T. ) ;
#3142=DIRECTION ( 'NONE',  ( 0.000000000000000000, 0.000000000000000000, -1.000000000000000000 ) ) ;
#3150=AXIS2_PLACEMENT_3D ( 'NONE', #7284, #321, #2393 ) ;
#3161=AXIS2_PLACEMENT_3D ( 'NONE', #1794, #1538, #6639 ) ;
#3181=DIRECTION ( 'NONE',  ( 0.000000000000000000, 0.4999999999999989453, -0.8660254037844392627 ) ) ;
#3188=DIRECTION ( 'NONE',  ( -1.000000000000000000, -0.000000000000000000, -0.000000000000000000 ) ) ;
#3226=ORIENTED_EDGE ( 'NONE', *, *, #1999, .F. ) ;
#3243=DIRECTION ( 'NONE',  ( -1.000000000000000000, 0.000000000000000000, 0.000000000000000000 ) ) ;
#3270=DIRECTION ( 'NONE',  ( 1.000000000000000000, 0.000000000000000000, 0.000000000000000000 ) ) ;
#3279=DIRECTION ( 'NONE',  ( 1.000000000000000000, 0.000000000000000000, 0.000000000000000000 ) ) ;
#3300=VECTOR ( 'NONE', #7458, 999.9999999999998863 ) ;
#3311=AXIS2_PLACEMENT_3D ( 'NONE', #8940, #4962, #6899 ) ;
#3332=DIRECTION ( 'NONE',  ( 0.000000000000000000, 0.000000000000000000, 1.000000000000000000 ) ) ;
#3341=ORIENTED_EDGE ( 'NONE', *, *, #10386, .F. ) ;
#3352=PRESENTATION_STYLE_ASSIGNMENT (( #6294 ) ) ;
#3366=VERTEX_POINT ( 'NONE', #3523 ) ;
#3375=DIRECTION ( 'NONE',  ( -1.000000000000000000, 0.000000000000000000, 0.000000000000000000 ) ) ;
#3389=EDGE_CURVE ( 'NONE', #1188, #4892, #5571, .T. ) ;
#3428=ORIENTED_EDGE ( 'NONE', *, *, #1999, .T. ) ;
#3444=ADVANCED_FACE ( 'NONE', ( #7756 ), #9791, .T. ) ;
#3516=CARTESIAN_POINT ( 'NONE',  ( 2.000000000000001776, -0.8865213383406691516, 1.535500000000002085 ) ) ;
#3523=CARTESIAN_POINT ( 'NONE',  ( 2.000000000000091926, -0.8865213383406727043, -1.535499999999998755 ) ) ;
#3533=CARTESIAN_POINT ( 'NONE',  ( 2.000000000000091926, 0.8865213383406691516, -1.535500000000002085 ) ) ;
#3534=ORIENTED_EDGE ( 'NONE', *, *, #10571, .T. ) ;
#3535=EDGE_CURVE ( 'NONE', #5702, #9004, #2819, .T. ) ;
#3542=ORIENTED_EDGE ( 'NONE', *, *, #12091, .T. ) ;
#3598=CARTESIAN_POINT ( 'NONE',  ( 4.200000000000001954, 0.000000000000000000, -1.734723475976807094E-14 ) ) ;
#3607=VECTOR ( 'NONE', #4061, 1000.000000000000000 ) ;
#3624=CIRCLE ( 'NONE', #6910, 2.000000000000000888 ) ;
#3665=LINE ( 'NONE', #10475, #3300 ) ;
#3672=EDGE_CURVE ( 'NONE', #4167, #10195, #11185, .T. ) ;
#3684=ORIENTED_EDGE ( 'NONE', *, *, #10386, .T. ) ;
#3689=CIRCLE ( 'NONE', #10867, 2.200000000000001066 ) ;
#3739=FACE_OUTER_BOUND ( 'NONE', #10941, .T. ) ;
#3824=DIRECTION ( 'NONE',  ( 0.000000000000000000, -0.4999999999999992784, 0.8660254037844389297 ) ) ;
#3833=CARTESIAN_POINT ( 'NONE',  ( 0.1999999999999987899, 0.000000000000000000, -1.734723475976807094E-14 ) ) ;
#3873=CARTESIAN_POINT ( 'NONE',  ( 2.000000000000001776, -0.8865213383406691516, 1.535500000000002085 ) ) ;
#3881=DIRECTION ( 'NONE',  ( 0.000000000000000000, 1.224646799147353207E-16, 1.000000000000000000 ) ) ;
#3884=VECTOR ( 'NONE', #318, 1000.000000000000000 ) ;
#3886=ORIENTED_EDGE ( 'NONE', *, *, #6204, .T. ) ;
#3920=ORIENTED_EDGE ( 'NONE', *, *, #11374, .F. ) ;
#3925=ORIENTED_EDGE ( 'NONE', *, *, #9381, .F. ) ;
#3960=ORIENTED_EDGE ( 'NONE', *, *, #8920, .F. ) ;
#3974=ORIENTED_EDGE ( 'NONE', *, *, #3025, .T. ) ;
#3991=DIRECTION ( 'NONE',  ( 0.000000000000000000, -0.5000000000000011102, -0.8660254037844379305 ) ) ;
#3995=VECTOR ( 'NONE', #10377, 1000.000000000000000 ) ;
#4024=ORIENTED_EDGE ( 'NONE', *, *, #12200, .T. ) ;
#4027=ORIENTED_EDGE ( 'NONE', *, *, #10967, .T. ) ;
#4031=PLANE ( 'NONE',  #354 ) ;
#4061=DIRECTION ( 'NONE',  ( 0.000000000000000000, -1.000000000000000000, 8.560894001270036306E-16 ) ) ;
#4123=FILL_AREA_STYLE ('',( #2987 ) ) ;
#4135=VECTOR ( 'NONE', #3824, 1000.000000000000227 ) ;
#4139=DIRECTION ( 'NONE',  ( -1.000000000000000000, 0.000000000000000000, 0.000000000000000000 ) ) ;
#4167=VERTEX_POINT ( 'NONE', #569 ) ;
#4170=VECTOR ( 'NONE', #7207, 1000.000000000000000 ) ;
#4180=VECTOR ( 'NONE', #6624, 1000.000000000000114 ) ;
#4189=( NAMED_UNIT ( * ) PLANE_ANGLE_UNIT ( ) SI_UNIT ( $, .RADIAN. ) );
#4190=LINE ( 'NONE', #1220, #9860 ) ;
#4194=PLANE ( 'NONE',  #8520 ) ;
#4223=ORIENTED_EDGE ( 'NONE', *, *, #4455, .T. ) ;
#4240=STYLED_ITEM ( 'NONE', ( #3352 ), #5724 ) ;
#4255=AXIS2_PLACEMENT_3D ( 'NONE', #982, #11815, #9857 ) ;
#4269=LINE ( 'NONE', #8194, #562 ) ;
#4313=FACE_OUTER_BOUND ( 'NONE', #1556, .T. ) ;
#4357=ORIENTED_EDGE ( 'NONE', *, *, #1282, .T. ) ;
#4361=ORIENTED_EDGE ( 'NONE', *, *, #8762, .F. ) ;
#4383=ADVANCED_FACE ( 'NONE', ( #12685, #8924 ), #4031, .T. ) ;
#4385=CARTESIAN_POINT ( 'NONE',  ( 2.000000000000001776, 1.773042676681341856, -3.469446951953614189E-15 ) ) ;
#4394=AXIS2_PLACEMENT_3D ( 'NONE', #208, #4139, #8056 ) ;
#4418=DIRECTION ( 'NONE',  ( 0.000000000000000000, 0.5000000000000012212, 0.8660254037844380415 ) ) ;
#4429=ORIENTED_EDGE ( 'NONE', *, *, #2359, .T. ) ;
#4451=PLANE ( 'NONE',  #1743 ) ;
#4455=EDGE_CURVE ( 'NONE', #10836, #1407, #8583, .T. ) ;
#4492=ORIENTED_EDGE ( 'NONE', *, *, #696, .F. ) ;
#4557=ORIENTED_EDGE ( 'NONE', *, *, #877, .F. ) ;
#4579=ORIENTED_EDGE ( 'NONE', *, *, #1787, .T. ) ;
#4581=CARTESIAN_POINT ( 'NONE',  ( 4.000000000000003553, 0.000000000000000000, 0.000000000000000000 ) ) ;
#4583=CIRCLE ( 'NONE', #3150, 0.2000000000000000944 ) ;
#4584=DIRECTION ( 'NONE',  ( -1.000000000000000000, 0.000000000000000000, 0.000000000000000000 ) ) ;
#4617=ORIENTED_EDGE ( 'NONE', *, *, #5824, .T. ) ;
#4621=AXIS2_PLACEMENT_3D ( 'NONE', #12729, #11822, #9736 ) ;
#4624=FACE_OUTER_BOUND ( 'NONE', #7011, .T. ) ;
#4653=DIRECTION ( 'NONE',  ( -1.000000000000000000, 0.000000000000000000, 0.000000000000000000 ) ) ;
#4656=DIRECTION ( 'NONE',  ( -0.7071067811865355823, 8.659560562355079537E-17, -0.7071067811865595631 ) ) ;
#4673=EDGE_LOOP ( 'NONE', ( #12082, #119, #5321, #4753 ) ) ;
#4697=ORIENTED_EDGE ( 'NONE', *, *, #2205, .F. ) ;
#4736=CIRCLE ( 'NONE', #6998, 2.200000000000001066 ) ;
#4752=CARTESIAN_POINT ( 'NONE',  ( 2.000000000000001776, 0.8865213383406727043, 1.535499999999998755 ) ) ;
#4753=ORIENTED_EDGE ( 'NONE', *, *, #12732, .T. ) ;
#4754=CARTESIAN_POINT ( 'NONE',  ( 2.000000000000001776, 1.773042676681341856, -3.469446951953614189E-15 ) ) ;
#4778=AXIS2_PLACEMENT_3D ( 'NONE', #10093, #5277, #1475 ) ;
#4820=AXIS2_PLACEMENT_3D ( 'NONE', #12682, #1783, #2777 ) ;
#4822=DIRECTION ( 'NONE',  ( 1.000000000000000000, 0.000000000000000000, 0.000000000000000000 ) ) ;
#4838=EDGE_CURVE ( 'NONE', #10019, #1763, #7695, .T. ) ;
#4849=VECTOR ( 'NONE', #4584, 1000.000000000000000 ) ;
#4853=ORIENTED_EDGE ( 'NONE', *, *, #852, .T. ) ;
#4860=DIRECTION ( 'NONE',  ( 0.000000000000000000, 1.467581828789149532E-15, 1.000000000000000000 ) ) ;
#4892=VERTEX_POINT ( 'NONE', #12536 ) ;
#4898=ORIENTED_EDGE ( 'NONE', *, *, #10360, .F. ) ;
#4900=ORIENTED_EDGE ( 'NONE', *, *, #217, .T. ) ;
#4947=VECTOR ( 'NONE', #3991, 1000.000000000000114 ) ;
#4950=VERTEX_POINT ( 'NONE', #9861 ) ;
#4962=DIRECTION ( 'NONE',  ( -1.000000000000000000, 0.000000000000000000, 0.000000000000000000 ) ) ;
#4965=LINE ( 'NONE', #8880, #4947 ) ;
#4994=VERTEX_POINT ( 'NONE', #5237 ) ;
#5008=EDGE_LOOP ( 'NONE', ( #12342, #3886, #919, #8081 ) ) ;
#5018=EDGE_CURVE ( 'NONE', #11532, #12678, #4269, .T. ) ;
#5029=DIRECTION ( 'NONE',  ( 0.000000000000000000, 0.5000000000000011102, 0.8660254037844379305 ) ) ;
#5033=DIRECTION ( 'NONE',  ( 0.000000000000000000, 0.000000000000000000, 1.000000000000000000 ) ) ;
#5041=CARTESIAN_POINT ( 'NONE',  ( 4.000000000000003553, 0.000000000000000000, 0.000000000000000000 ) ) ;
#5083=VERTEX_POINT ( 'NONE', #12206 ) ;
#5111=DIRECTION ( 'NONE',  ( 0.000000000000000000, -0.4999999999999989453, 0.8660254037844391517 ) ) ;
#5166=CARTESIAN_POINT ( 'NONE',  ( 2.000000000000091926, 0.8865213383406691516, -1.535500000000002085 ) ) ;
#5189=ORIENTED_EDGE ( 'NONE', *, *, #10805, .T. ) ;
#5214=CARTESIAN_POINT ( 'NONE',  ( 2.000000000000001776, -1.773042676681341856, 3.469446951953614189E-15 ) ) ;
#5237=CARTESIAN_POINT ( 'NONE',  ( 4.000000000000003553, 4.286263797015725748E-16, -3.500000000000000000 ) ) ;
#5241=PRODUCT ( 'socket head cap screw_iso_ISO 4762 M4 x 30 - 20N', 'socket head cap screw_iso_ISO 4762 M4 x 30 - 20N', '', ( #2025 ) ) ;
#5256=ORIENTED_EDGE ( 'NONE', *, *, #10360, .T. ) ;
#5274=AXIS2_PLACEMENT_3D ( 'NONE', #10520, #2618, #5509 ) ;
#5277=DIRECTION ( 'NONE',  ( 1.000000000000000000, -0.000000000000000000, -0.000000000000000000 ) ) ;
#5279=CARTESIAN_POINT ( 'NONE',  ( 0.000000000000000000, 0.8865213383406727043, 1.535499999999998755 ) ) ;
#5305=FACE_OUTER_BOUND ( 'NONE', #12480, .T. ) ;
#5320=ORIENTED_EDGE ( 'NONE', *, *, #9493, .T. ) ;
#5321=ORIENTED_EDGE ( 'NONE', *, *, #450, .T. ) ;
#5348=DIRECTION ( 'NONE',  ( 0.000000000000000000, 0.000000000000000000, 1.000000000000000000 ) ) ;
#5350=FACE_OUTER_BOUND ( 'NONE', #5999, .T. ) ;
#5395=EDGE_LOOP ( 'NONE', ( #11182, #8165, #6920 ) ) ;
#5406=VECTOR ( 'NONE', #11160, 1000.000000000000000 ) ;
#5428=CARTESIAN_POINT ( 'NONE',  ( 33.61000000000001364, 0.000000000000000000, 0.000000000000000000 ) ) ;
#5435=ORIENTED_EDGE ( 'NONE', *, *, #9372, .F. ) ;
#5457=DIRECTION ( 'NONE',  ( 0.000000000000000000, 0.000000000000000000, -1.000000000000000000 ) ) ;
#5459=CARTESIAN_POINT ( 'NONE',  ( 1.999999999999994893, -1.329782007511007169, -0.7677499999999976010 ) ) ;
#5483=DIRECTION ( 'NONE',  ( 0.000000000000000000, -0.5000000000000012212, -0.8660254037844380415 ) ) ;
#5509=DIRECTION ( 'NONE',  ( 0.000000000000000000, 0.000000000000000000, 1.000000000000000000 ) ) ;
#5510=DIRECTION ( 'NONE',  ( -1.000000000000000000, 0.000000000000000000, 0.000000000000000000 ) ) ;
#5522=( NAMED_UNIT ( * ) SI_UNIT ( $, .STERADIAN. ) SOLID_ANGLE_UNIT ( ) );
#5537=ORIENTED_EDGE ( 'NONE', *, *, #7837, .F. ) ;
#5571=LINE ( 'NONE', #11242, #1505 ) ;
#5601=ORIENTED_EDGE ( 'NONE', *, *, #1145, .T. ) ;
#5603=FACE_BOUND ( 'NONE', #8737, .T. ) ;
#5642=CARTESIAN_POINT ( 'NONE',  ( 0.000000000000000000, -0.8865213383406691516, 1.535500000000002085 ) ) ;
#5675=DIRECTION ( 'NONE',  ( -1.000000000000000000, 0.000000000000000000, 0.000000000000000000 ) ) ;
#5702=VERTEX_POINT ( 'NONE', #11326 ) ;
#5707=CARTESIAN_POINT ( 'NONE',  ( 0.000000000000000000, 0.000000000000000000, 0.000000000000000000 ) ) ;
#5710=ORIENTED_EDGE ( 'NONE', *, *, #7203, .F. ) ;
#5724=MANIFOLD_SOLID_BREP ( 'Hex', #8272 ) ;
#5759=CARTESIAN_POINT ( 'NONE',  ( 2.000000000000001776, 1.773042676681341856, -3.469446951953614189E-15 ) ) ;
#5794=EDGE_CURVE ( 'NONE', #2957, #8146, #8160, .T. ) ;
#5815=DIRECTION ( 'NONE',  ( -1.000000000000000000, 0.000000000000000000, 0.000000000000000000 ) ) ;
#5816=CIRCLE ( 'NONE', #1292, 2.000000000000000888 ) ;
#5824=EDGE_CURVE ( 'NONE', #9207, #1632, #12287, .T. ) ;
#5829=PLANE ( 'NONE',  #1413 ) ;
#5877=VECTOR ( 'NONE', #201, 1000.000000000000114 ) ;
#5890=DIRECTION ( 'NONE',  ( 0.000000000000000000, 1.000000000000000000, -1.467581828789149335E-15 ) ) ;
#5942=PLANE ( 'NONE',  #4255 ) ;
#5974=ORIENTED_EDGE ( 'NONE', *, *, #3140, .T. ) ;
#5980=ORIENTED_EDGE ( 'NONE', *, *, #7545, .F. ) ;
#5996=LINE ( 'NONE', #9911, #8426 ) ;
#5999=EDGE_LOOP ( 'NONE', ( #10802, #7148 ) ) ;
#6003=LINE ( 'NONE', #9667, #789 ) ;
#6028=DIRECTION ( 'NONE',  ( 0.000000000000000000, 0.000000000000000000, 1.000000000000000000 ) ) ;
#6044=ADVANCED_FACE ( 'NONE', ( #2012 ), #5942, .F. ) ;
#6050=DIRECTION ( 'NONE',  ( -1.000000000000000000, 0.000000000000000000, 0.000000000000000000 ) ) ;
#6053=SURFACE_SIDE_STYLE ('',( #7916 ) ) ;
#6072=FACE_OUTER_BOUND ( 'NONE', #7902, .T. ) ;
#6074=ORIENTED_EDGE ( 'NONE', *, *, #10121, .F. ) ;
#6087=EDGE_LOOP ( 'NONE', ( #4492, #10648 ) ) ;
#6116=DIRECTION ( 'NONE',  ( 0.000000000000000000, 0.000000000000000000, 1.000000000000000000 ) ) ;
#6187=ADVANCED_BREP_SHAPE_REPRESENTATION ( '', ( #5724, #12422 ), #3119 ) ;
#6190=( GEOMETRIC_REPRESENTATION_CONTEXT ( 3 ) GLOBAL_UNCERTAINTY_ASSIGNED_CONTEXT ( ( #11399 ) ) GLOBAL_UNIT_ASSIGNED_CONTEXT ( ( #255, #4189, #12057 ) ) REPRESENTATION_CONTEXT ( 'NONE', 'WORKASPACE' ) );
#6204=EDGE_CURVE ( 'NONE', #12214, #6728, #2475, .T. ) ;
#6246=CARTESIAN_POINT ( 'NONE',  ( 2.000000000000001776, 0.000000000000000000, 0.000000000000000000 ) ) ;
#6260=DIRECTION ( 'NONE',  ( 0.000000000000000000, 0.000000000000000000, -1.000000000000000000 ) ) ;
#6294=SURFACE_STYLE_USAGE ( .BOTH. , #6356 ) ;
#6356=SURFACE_SIDE_STYLE ('',( #2571 ) ) ;
#6404=ORIENTED_EDGE ( 'NONE', *, *, #12091, .F. ) ;
#6420=PLANE ( 'NONE',  #10375 ) ;
#6428=DIRECTION ( 'NONE',  ( 1.000000000000000000, 0.000000000000000000, 0.000000000000000000 ) ) ;
#6470=DIRECTION ( 'NONE',  ( -1.000000000000000000, 0.000000000000000000, 0.000000000000000000 ) ) ;
#6489=ORIENTED_EDGE ( 'NONE', *, *, #450, .F. ) ;
#6492=ORIENTED_EDGE ( 'NONE', *, *, #9231, .T. ) ;
#6508=AXIS2_PLACEMENT_3D ( 'NONE', #9011, #3375, #7292 ) ;
#6512=DIRECTION ( 'NONE',  ( 0.000000000000000000, 0.000000000000000000, 1.000000000000000000 ) ) ;
#6564=CIRCLE ( 'NONE', #8394, 1.535500000000000087 ) ;
#6574=DIRECTION ( 'NONE',  ( -1.000000000000000000, 0.000000000000000000, 0.000000000000000000 ) ) ;
#6624=DIRECTION ( 'NONE',  ( 0.000000000000000000, -0.5000000000000011102, -0.8660254037844379305 ) ) ;
#6639=DIRECTION ( 'NONE',  ( 0.000000000000000000, 0.000000000000000000, -1.000000000000000000 ) ) ;
#6645=VECTOR ( 'NONE', #11014, 1000.000000000000000 ) ;
#6647=FACE_OUTER_BOUND ( 'NONE', #8663, .T. ) ;
#6651=ORIENTED_EDGE ( 'NONE', *, *, #9381, .T. ) ;
#6691=PLANE ( 'NONE',  #12736 ) ;
#6717=( GEOMETRIC_REPRESENTATION_CONTEXT ( 3 ) GLOBAL_UNCERTAINTY_ASSIGNED_CONTEXT ( ( #10698 ) ) GLOBAL_UNIT_ASSIGNED_CONTEXT ( ( #9365, #10470, #5522 ) ) REPRESENTATION_CONTEXT ( 'NONE', 'WORKASPACE' ) );
#6728=VERTEX_POINT ( 'NONE', #692 ) ;
#6735=EDGE_LOOP ( 'NONE', ( #6831, #473, #1133, #8155, #9349 ) ) ;
#6762=VECTOR ( 'NONE', #6924, 1000.000000000000000 ) ;
#6773=CYLINDRICAL_SURFACE ( 'NONE', #11150, 3.500000000000000000 ) ;
#6807=EDGE_LOOP ( 'NONE', ( #7223, #1569, #10597, #4557 ) ) ;
#6831=ORIENTED_EDGE ( 'NONE', *, *, #12590, .T. ) ;
#6837=CARTESIAN_POINT ( 'NONE',  ( 4.200000000000001954, 0.000000000000000000, -1.734723475976807094E-14 ) ) ;
#6847=CARTESIAN_POINT ( 'NONE',  ( -31.74999999999995026, 0.000000000000000000, 1.999999999999983569 ) ) ;
#6899=DIRECTION ( 'NONE',  ( 0.000000000000000000, 0.000000000000000000, 1.000000000000000000 ) ) ;
#6910=AXIS2_PLACEMENT_3D ( 'NONE', #5428, #7490, #10567 ) ;
#6918=ADVANCED_FACE ( 'NONE', ( #297 ), #6420, .F. ) ;
#6920=ORIENTED_EDGE ( 'NONE', *, *, #12200, .F. ) ;
#6924=DIRECTION ( 'NONE',  ( -0.5000000000000061062, 0.000000000000000000, 0.8660254037844351549 ) ) ;
#6960=ORIENTED_EDGE ( 'NONE', *, *, #8008, .F. ) ;
#6971=AXIS2_PLACEMENT_3D ( 'NONE', #1826, #10898, #10705 ) ;
#6986=CIRCLE ( 'NONE', #10255, 1.535500000000000087 ) ;
#6987=CARTESIAN_POINT ( 'NONE',  ( 2.000000000000001776, -0.8865213383406691516, 1.535500000000002085 ) ) ;
#6998=AXIS2_PLACEMENT_3D ( 'NONE', #5041, #3188, #8830 ) ;
#7011=EDGE_LOOP ( 'NONE', ( #3920, #4898, #682, #1260, #4579 ) ) ;
#7034=CYLINDRICAL_SURFACE ( 'NONE', #6508, 2.000000000000000888 ) ;
#7058=ORIENTED_EDGE ( 'NONE', *, *, #154, .T. ) ;
#7090=CARTESIAN_POINT ( 'NONE',  ( 2.000000000000001776, 0.000000000000000000, 0.000000000000000000 ) ) ;
#7101=VECTOR ( 'NONE', #10902, 1000.000000000000227 ) ;
#7137=ORIENTED_EDGE ( 'NONE', *, *, #4838, .T. ) ;
#7142=VERTEX_POINT ( 'NONE', #9545 ) ;
#7148=ORIENTED_EDGE ( 'NONE', *, *, #10823, .F. ) ;
#7195=VECTOR ( 'NONE', #6470, 1000.000000000000000 ) ;
#7203=EDGE_CURVE ( 'NONE', #5083, #9004, #11821, .T. ) ;
#7204=EDGE_LOOP ( 'NONE', ( #6404, #3974, #2252, #4617 ) ) ;
#7207=DIRECTION ( 'NONE',  ( 0.000000000000000000, 1.000000000000000000, -1.467581828789149335E-15 ) ) ;
#7217=AXIS2_PLACEMENT_3D ( 'NONE', #7090, #3243, #6116 ) ;
#7223=ORIENTED_EDGE ( 'NONE', *, *, #12732, .F. ) ;
#7261=CARTESIAN_POINT ( 'NONE',  ( 2.000000000000001776, 0.000000000000000000, 0.000000000000000000 ) ) ;
#7284=CARTESIAN_POINT ( 'NONE',  ( 0.1999999999999987899, 0.000000000000000000, 3.299999999999982503 ) ) ;
#7287=CARTESIAN_POINT ( 'NONE',  ( 0.000000000000000000, 0.000000000000000000, 0.000000000000000000 ) ) ;
#7292=DIRECTION ( 'NONE',  ( 0.000000000000000000, 0.000000000000000000, 1.000000000000000000 ) ) ;
#7299=ADVANCED_FACE ( 'NONE', ( #152 ), #7734, .T. ) ;
#7315=AXIS2_PLACEMENT_3D ( 'NONE', #12432, #12240, #2579 ) ;
#7348=CARTESIAN_POINT ( 'NONE',  ( 0.000000000000000000, -0.8865213383406691516, 1.535500000000002085 ) ) ;
#7373=CARTESIAN_POINT ( 'NONE',  ( -31.74999999999995026, 0.000000000000000000, -1.734723475976807094E-14 ) ) ;
#7392=DIRECTION ( 'NONE',  ( 0.000000000000000000, 0.000000000000000000, 1.000000000000000000 ) ) ;
#7458=DIRECTION ( 'NONE',  ( 0.000000000000000000, -0.5000000000000012212, -0.8660254037844380415 ) ) ;
#7490=DIRECTION ( 'NONE',  ( -1.000000000000000000, 0.000000000000000000, 0.000000000000000000 ) ) ;
#7513=ORIENTED_EDGE ( 'NONE', *, *, #1145, .F. ) ;
#7532=ORIENTED_EDGE ( 'NONE', *, *, #10892, .T. ) ;
#7545=EDGE_CURVE ( 'NONE', #6728, #4892, #3624, .T. ) ;
#7564=CARTESIAN_POINT ( 'NONE',  ( 34.00000000000000000, 0.000000000000000000, 1.609999999999982778 ) ) ;
#7573=ORIENTED_EDGE ( 'NONE', *, *, #2969, .T. ) ;
#7575=CARTESIAN_POINT ( 'NONE',  ( 9.714451465470119729E-14, 0.8865213383406691516, -1.535500000000002085 ) ) ;
#7580=VERTEX_POINT ( 'NONE', #10443 ) ;
#7588=AXIS2_PLACEMENT_3D ( 'NONE', #4, #6050, #9962 ) ;
#7628=STYLED_ITEM ( 'NONE', ( #2064 ), #6187 ) ;
#7641=CARTESIAN_POINT ( 'NONE',  ( 2.000000000000001776, -0.8865213383406691516, 1.535500000000002085 ) ) ;
#7673=CARTESIAN_POINT ( 'NONE',  ( -31.74999999999995026, 0.000000000000000000, -1.734723475976807094E-14 ) ) ;
#7695=LINE ( 'NONE', #8662, #11660 ) ;
#7734=TOROIDAL_SURFACE ( 'NONE', #2816, 3.299999999999999822, 0.2000000000000000111 ) ;
#7756=FACE_OUTER_BOUND ( 'NONE', #636, .T. ) ;
#7762=DIRECTION ( 'NONE',  ( -1.000000000000000000, 0.000000000000000000, 0.000000000000000000 ) ) ;
#7773=EDGE_CURVE ( 'NONE', #12678, #10836, #8954, .T. ) ;
#7776=CARTESIAN_POINT ( 'NONE',  ( 4.000000000000003553, 3.499999999999999556, 0.000000000000000000 ) ) ;
#7821=AXIS2_PLACEMENT_3D ( 'NONE', #11407, #2586, #6512 ) ;
#7837=EDGE_CURVE ( 'NONE', #10019, #1407, #1351, .T. ) ;
#7845=PLANE ( 'NONE',  #12409 ) ;
#7855=ADVANCED_FACE ( 'NONE', ( #5350 ), #4194, .T. ) ;
#7896=ADVANCED_FACE ( 'NONE', ( #2272 ), #7034, .T. ) ;
#7902=EDGE_LOOP ( 'NONE', ( #11658, #10742, #2316, #5320, #12745 ) ) ;
#7911=CARTESIAN_POINT ( 'NONE',  ( 2.000000000000091926, 0.000000000000000000, -1.535499999999998755 ) ) ;
#7916=SURFACE_STYLE_FILL_AREA ( #4123 ) ;
#7917=DIRECTION ( 'NONE',  ( 0.000000000000000000, -0.4999999999999992784, 0.8660254037844389297 ) ) ;
#7930=ORIENTED_EDGE ( 'NONE', *, *, #7773, .T. ) ;
#7931=ORIENTED_EDGE ( 'NONE', *, *, #10834, .T. ) ;
#7942=CARTESIAN_POINT ( 'NONE',  ( 2.000000000000001776, -1.773042676681341856, 3.469446951953614189E-15 ) ) ;
#7964=FACE_OUTER_BOUND ( 'NONE', #1710, .T. ) ;
#7971=ADVANCED_FACE ( 'NONE', ( #6647 ), #4451, .F. ) ;
#8003=PLANE ( 'NONE',  #9348 ) ;
#8008=EDGE_CURVE ( 'NONE', #12678, #1792, #2590, .T. ) ;
#8025=ORIENTED_EDGE ( 'NONE', *, *, #1262, .F. ) ;
#8040=CARTESIAN_POINT ( 'NONE',  ( 33.61000000000001364, 0.000000000000000000, 0.000000000000000000 ) ) ;
#8048=CARTESIAN_POINT ( 'NONE',  ( 34.00000000000000000, 1.610000000000000320, -1.734723475976807094E-14 ) ) ;
#8056=DIRECTION ( 'NONE',  ( 0.000000000000000000, 0.000000000000000000, 1.000000000000000000 ) ) ;
#8058=DIRECTION ( 'NONE',  ( 0.000000000000000000, 0.8660254037844392627, 0.4999999999999990008 ) ) ;
#8081=ORIENTED_EDGE ( 'NONE', *, *, #3389, .F. ) ;
#8086=VECTOR ( 'NONE', #9540, 1000.000000000000000 ) ;
#8103=DIRECTION ( 'NONE',  ( 0.000000000000000000, 0.000000000000000000, -1.000000000000000000 ) ) ;
#8104=ORIENTED_EDGE ( 'NONE', *, *, #1285, .T. ) ;
#8146=VERTEX_POINT ( 'NONE', #8813 ) ;
#8155=ORIENTED_EDGE ( 'NONE', *, *, #8553, .F. ) ;
#8160=CIRCLE ( 'NONE', #11864, 2.000000000000000888 ) ;
#8165=ORIENTED_EDGE ( 'NONE', *, *, #8553, .T. ) ;
#8192=CIRCLE ( 'NONE', #6971, 0.2000000000000000944 ) ;
#8194=CARTESIAN_POINT ( 'NONE',  ( 2.000000000000001776, 1.773042676681341856, -3.469446951953614189E-15 ) ) ;
#8218=CIRCLE ( 'NONE', #2686, 0.2000000000000000944 ) ;
#8223=VECTOR ( 'NONE', #3107, 1000.000000000000114 ) ;
#8224=ORIENTED_EDGE ( 'NONE', *, *, #5018, .F. ) ;
#8249=PLANE ( 'NONE',  #12390 ) ;
#8252=CARTESIAN_POINT ( 'NONE',  ( 2.000000000000001776, -1.773042676681341856, 3.469446951953614189E-15 ) ) ;
#8272=CLOSED_SHELL ( 'NONE', ( #8370, #2516, #9460, #9435, #11302, #3444, #660, #11843, #4383, #7896, #769, #7855, #141, #7299, #1353, #8528, #11965, #1339, #6044, #6918, #7971, #12363, #10674, #8598, #11137, #12433, #2413 ) ) ;
#8308=DIRECTION ( 'NONE',  ( -1.000000000000000000, 0.000000000000000000, 0.000000000000000000 ) ) ;
#8329=LINE ( 'NONE', #3516, #7195 ) ;
#8355=COLOUR_RGB ( '', 0.40784314, 0.44705882, 0.49803922) ;
#8370=ADVANCED_FACE ( 'NONE', ( #1469 ), #106, .F. ) ;
#8394=AXIS2_PLACEMENT_3D ( 'NONE', #10456, #5510, #12411 ) ;
#8426=VECTOR ( 'NONE', #10953, 1000.000000000000000 ) ;
#8435=AXIS2_PLACEMENT_3D ( 'NONE', #6246, #10154, #1346 ) ;
#8469=ORIENTED_EDGE ( 'NONE', *, *, #696, .T. ) ;
#8473=AXIS2_PLACEMENT_3D ( 'NONE', #3873, #9965, #5029 ) ;
#8501=PLANE ( 'NONE',  #11102 ) ;
#8520=AXIS2_PLACEMENT_3D ( 'NONE', #8048, #136, #1165 ) ;
#8528=ADVANCED_FACE ( 'NONE', ( #10840 ), #8003, .F. ) ;
#8536=VERTEX_POINT ( 'NONE', #11951 ) ;
#8553=EDGE_CURVE ( 'NONE', #11062, #5702, #10709, .T. ) ;
#8583=CIRCLE ( 'NONE', #8991, 1.535500000000000087 ) ;
#8598=ADVANCED_FACE ( 'NONE', ( #9797 ), #9925, .F. ) ;
#8631=DIRECTION ( 'NONE',  ( -1.000000000000000000, 0.000000000000000000, 0.000000000000000000 ) ) ;
#8633=LINE ( 'NONE', #2796, #610 ) ;
#8638=TOROIDAL_SURFACE ( 'NONE', #2052, 2.200000000000001066, 0.2000000000000000111 ) ;
#8662=CARTESIAN_POINT ( 'NONE',  ( 2.000000000000001776, -1.773042676681341856, 3.469446951953614189E-15 ) ) ;
#8663=EDGE_LOOP ( 'NONE', ( #7532, #10190, #12216 ) ) ;
#8685=FACE_OUTER_BOUND ( 'NONE', #11770, .T. ) ;
#8698=DIRECTION ( 'NONE',  ( -0.5000000000000061062, 1.060575238724902601E-16, -0.8660254037844351549 ) ) ;
#8703=FACE_OUTER_BOUND ( 'NONE', #7204, .T. ) ;
#8737=EDGE_LOOP ( 'NONE', ( #1949, #11386, #6651, #4429, #1406, #9772 ) ) ;
#8748=DIRECTION ( 'NONE',  ( 0.000000000000000000, 0.000000000000000000, -1.000000000000000000 ) ) ;
#8754=DIRECTION ( 'NONE',  ( 0.000000000000000000, -1.000000000000000000, 8.560894001270036306E-16 ) ) ;
#8762=EDGE_CURVE ( 'NONE', #7580, #9207, #784, .T. ) ;
#8813=CARTESIAN_POINT ( 'NONE',  ( 4.200000000000001954, 0.000000000000000000, 1.999999999999983569 ) ) ;
#8830=DIRECTION ( 'NONE',  ( 0.000000000000000000, 0.000000000000000000, -1.000000000000000000 ) ) ;
#8847=DIRECTION ( 'NONE',  ( 0.000000000000000000, -1.000000000000000000, 1.467581828789149532E-15 ) ) ;
#8880=CARTESIAN_POINT ( 'NONE',  ( 2.000000000000001776, -0.8865213383406691516, 1.535500000000002085 ) ) ;
#8882=CARTESIAN_POINT ( 'NONE',  ( -31.74999999999995026, 4.286263797015736595E-16, -3.500000000000017319 ) ) ;
#8920=EDGE_CURVE ( 'NONE', #8146, #11433, #1423, .T. ) ;
#8924=FACE_OUTER_BOUND ( 'NONE', #6087, .T. ) ;
#8929=ORIENTED_EDGE ( 'NONE', *, *, #5794, .F. ) ;
#8940=CARTESIAN_POINT ( 'NONE',  ( 34.00000000000000000, 0.000000000000000000, -1.734723475976807094E-14 ) ) ;
#8954=LINE ( 'NONE', #5166, #3607 ) ;
#8978=DIRECTION ( 'NONE',  ( -1.000000000000000000, 0.000000000000000000, 0.000000000000000000 ) ) ;
#8991=AXIS2_PLACEMENT_3D ( 'NONE', #7261, #11181, #6028 ) ;
#9004=VERTEX_POINT ( 'NONE', #1100 ) ;
#9011=CARTESIAN_POINT ( 'NONE',  ( -31.74999999999995026, 0.000000000000000000, -1.734723475976807094E-14 ) ) ;
#9022=FACE_OUTER_BOUND ( 'NONE', #10922, .T. ) ;
#9034=CONICAL_SURFACE ( 'NONE', #12135, 1.610000000000000098, 0.7853981633974652654 ) ;
#9070=CARTESIAN_POINT ( 'NONE',  ( 4.000000000000003553, 0.000000000000000000, 0.000000000000000000 ) ) ;
#9077=AXIS2_PLACEMENT_3D ( 'NONE', #1934, #10946, #5033 ) ;
#9094=AXIS2_PLACEMENT_3D ( 'NONE', #2282, #1298, #6260 ) ;
#9128=VECTOR ( 'NONE', #5890, 1000.000000000000000 ) ;
#9198=CARTESIAN_POINT ( 'NONE',  ( 2.000000000000001776, 0.000000000000000000, 0.000000000000000000 ) ) ;
#9207=VERTEX_POINT ( 'NONE', #11153 ) ;
#9231=EDGE_CURVE ( 'NONE', #7142, #1792, #456, .T. ) ;
#9249=EDGE_LOOP ( 'NONE', ( #4697, #7573, #1277 ) ) ;
#9291=AXIS2_PLACEMENT_3D ( 'NONE', #9198, #1280, #446 ) ;
#9348=AXIS2_PLACEMENT_3D ( 'NONE', #6987, #4860, #8847 ) ;
#9349=ORIENTED_EDGE ( 'NONE', *, *, #10121, .T. ) ;
#9365=( LENGTH_UNIT ( ) NAMED_UNIT ( * ) SI_UNIT ( .MILLI., .METRE. ) );
#9372=EDGE_CURVE ( 'NONE', #3366, #10769, #12446, .T. ) ;
#9381=EDGE_CURVE ( 'NONE', #2497, #1763, #2505, .T. ) ;
#9435=ADVANCED_FACE ( 'NONE', ( #10807 ), #607, .T. ) ;
#9455=FACE_OUTER_BOUND ( 'NONE', #5395, .T. ) ;
#9460=ADVANCED_FACE ( 'NONE', ( #11600 ), #8638, .F. ) ;
#9492=CIRCLE ( 'NONE', #9291, 1.535500000000000087 ) ;
#9493=EDGE_CURVE ( 'NONE', #1407, #3366, #11008, .T. ) ;
#9497=DIRECTION ( 'NONE',  ( 0.000000000000000000, -0.8660254037844390407, -0.4999999999999992784 ) ) ;
#9515=DIRECTION ( 'NONE',  ( 1.000000000000000000, 0.000000000000000000, 0.000000000000000000 ) ) ;
#9540=DIRECTION ( 'NONE',  ( 0.000000000000000000, 1.000000000000000000, -1.467581828789149335E-15 ) ) ;
#9545=CARTESIAN_POINT ( 'NONE',  ( 0.000000000000000000, 1.773042676681341856, -3.469446951953614189E-15 ) ) ;
#9559=DIRECTION ( 'NONE',  ( 0.000000000000000000, 0.4999999999999992784, -0.8660254037844390407 ) ) ;
#9578=CARTESIAN_POINT ( 'NONE',  ( 2.000000000000091926, -0.8865213383406727043, -1.535499999999998755 ) ) ;
#9627=AXIS2_PLACEMENT_3D ( 'NONE', #11808, #3057, #3881 ) ;
#9667=CARTESIAN_POINT ( 'NONE',  ( 2.000000000000001776, -0.8865213383406691516, 1.535500000000002085 ) ) ;
#9693=LINE ( 'NONE', #888, #4170 ) ;
#9726=ORIENTED_EDGE ( 'NONE', *, *, #10571, .F. ) ;
#9730=CARTESIAN_POINT ( 'NONE',  ( 2.000000000000001776, 0.000000000000000000, 1.535500000000000087 ) ) ;
#9736=DIRECTION ( 'NONE',  ( 0.000000000000000000, 0.000000000000000000, -1.000000000000000000 ) ) ;
#9772=ORIENTED_EDGE ( 'NONE', *, *, #9231, .F. ) ;
#9773=FACE_OUTER_BOUND ( 'NONE', #1419, .T. ) ;
#9791=CYLINDRICAL_SURFACE ( 'NONE', #690, 3.500000000000000000 ) ;
#9797=FACE_OUTER_BOUND ( 'NONE', #11124, .T. ) ;
#9827=AXIS2_PLACEMENT_3D ( 'NONE', #8040, #10743, #961 ) ;
#9853=ORIENTED_EDGE ( 'NONE', *, *, #7773, .F. ) ;
#9857=DIRECTION ( 'NONE',  ( 0.000000000000000000, 1.000000000000000000, -8.560894001270036306E-16 ) ) ;
#9859=CIRCLE ( 'NONE', #7217, 1.535500000000000087 ) ;
#9860=VECTOR ( 'NONE', #3181, 1000.000000000000114 ) ;
#9861=CARTESIAN_POINT ( 'NONE',  ( 2.000000000000001776, 1.773042676681341856, -3.469446951953614189E-15 ) ) ;
#9877=DIRECTION ( 'NONE',  ( 0.000000000000000000, 0.000000000000000000, 1.000000000000000000 ) ) ;
#9911=CARTESIAN_POINT ( 'NONE',  ( 2.000000000000001776, 1.773042676681341856, -3.469446951953614189E-15 ) ) ;
#9925=PLANE ( 'NONE',  #4621 ) ;
#9962=DIRECTION ( 'NONE',  ( 0.000000000000000000, 0.000000000000000000, 1.000000000000000000 ) ) ;
#9965=DIRECTION ( 'NONE',  ( 0.000000000000000000, 0.8660254037844380415, -0.5000000000000012212 ) ) ;
#10001=CARTESIAN_POINT ( 'NONE',  ( 2.000000000000001776, 0.000000000000000000, 0.000000000000000000 ) ) ;
#10003=CARTESIAN_POINT ( 'NONE',  ( 34.00000000000000000, 0.000000000000000000, -1.734723475976807094E-14 ) ) ;
#10013=ORIENTED_EDGE ( 'NONE', *, *, #1285, .F. ) ;
#10019=VERTEX_POINT ( 'NONE', #7942 ) ;
#10052=VECTOR ( 'NONE', #8631, 1000.000000000000000 ) ;
#10056=PRODUCT_DEFINITION_SHAPE ( 'NONE', 'NONE',  #2740 ) ;
#10061=ORIENTED_EDGE ( 'NONE', *, *, #12170, .F. ) ;
#10093=CARTESIAN_POINT ( 'NONE',  ( 0.1999999999999987899, 0.000000000000000000, -1.734723475976807094E-14 ) ) ;
#10094=SHAPE_REPRESENTATION ( 'socket head cap screw_iso_ISO 4762 M4 x 30 - 20N', ( #12422 ), #3119 ) ;
#10096=AXIS2_PLACEMENT_3D ( 'NONE', #4581, #6574, #10291 ) ;
#10121=EDGE_CURVE ( 'NONE', #11062, #2497, #8329, .T. ) ;
#10154=DIRECTION ( 'NONE',  ( -1.000000000000000000, 0.000000000000000000, 0.000000000000000000 ) ) ;
#10190=ORIENTED_EDGE ( 'NONE', *, *, #9493, .F. ) ;
#10195=VERTEX_POINT ( 'NONE', #2485 ) ;
#10246=ORIENTED_EDGE ( 'NONE', *, *, #217, .F. ) ;
#10255=AXIS2_PLACEMENT_3D ( 'NONE', #10300, #8978, #161 ) ;
#10266=ORIENTED_EDGE ( 'NONE', *, *, #3140, .F. ) ;
#10291=DIRECTION ( 'NONE',  ( 0.000000000000000000, 0.000000000000000000, 1.000000000000000000 ) ) ;
#10300=CARTESIAN_POINT ( 'NONE',  ( 2.000000000000001776, 0.000000000000000000, 0.000000000000000000 ) ) ;
#10337=FILL_AREA_STYLE ('',( #12233 ) ) ;
#10360=EDGE_CURVE ( 'NONE', #4950, #7142, #5996, .T. ) ;
#10363=ORIENTED_EDGE ( 'NONE', *, *, #3672, .T. ) ;
#10373=CARTESIAN_POINT ( 'NONE',  ( 34.00000000000000000, 1.971681346627238735E-16, -1.610000000000017417 ) ) ;
#10375=AXIS2_PLACEMENT_3D ( 'NONE', #2306, #233, #4418 ) ;
#10377=DIRECTION ( 'NONE',  ( -1.000000000000000000, 0.000000000000000000, 0.000000000000000000 ) ) ;
#10384=ORIENTED_EDGE ( 'NONE', *, *, #12170, .T. ) ;
#10386=EDGE_CURVE ( 'NONE', #11433, #11940, #4736, .T. ) ;
#10428=CARTESIAN_POINT ( 'NONE',  ( 2.000000000000091926, 0.8865213383406691516, -1.535500000000002085 ) ) ;
#10443=CARTESIAN_POINT ( 'NONE',  ( 4.000000000000003553, 0.000000000000000000, 3.500000000000000000 ) ) ;
#10456=CARTESIAN_POINT ( 'NONE',  ( 2.000000000000001776, 0.000000000000000000, 0.000000000000000000 ) ) ;
#10470=( NAMED_UNIT ( * ) PLANE_ANGLE_UNIT ( ) SI_UNIT ( $, .RADIAN. ) );
#10475=CARTESIAN_POINT ( 'NONE',  ( 2.000000000000001776, 1.773042676681341856, -3.469446951953614189E-15 ) ) ;
#10515=ORIENTED_EDGE ( 'NONE', *, *, #1262, .T. ) ;
#10520=CARTESIAN_POINT ( 'NONE',  ( 0.1999999999999987899, 0.000000000000000000, -1.734723475976807094E-14 ) ) ;
#10567=DIRECTION ( 'NONE',  ( 0.000000000000000000, 0.000000000000000000, 1.000000000000000000 ) ) ;
#10571=EDGE_CURVE ( 'NONE', #8536, #10836, #8633, .T. ) ;
#10582=CARTESIAN_POINT ( 'NONE',  ( -31.74999999999995026, 0.000000000000000000, -1.734723475976807094E-14 ) ) ;
#10597=ORIENTED_EDGE ( 'NONE', *, *, #10977, .F. ) ;
#10622=CARTESIAN_POINT ( 'NONE',  ( 2.000000000000001776, 1.773042676681341856, -3.469446951953614189E-15 ) ) ;
#10648=ORIENTED_EDGE ( 'NONE', *, *, #3025, .F. ) ;
#10667=CARTESIAN_POINT ( 'NONE',  ( 2.000000000000001776, 1.773042676681341856, -3.469446951953614189E-15 ) ) ;
#10674=ADVANCED_FACE ( 'NONE', ( #9455 ), #8501, .F. ) ;
#10684=DIRECTION ( 'NONE',  ( -1.000000000000000000, 0.000000000000000000, 0.000000000000000000 ) ) ;
#10698=UNCERTAINTY_MEASURE_WITH_UNIT (LENGTH_MEASURE( 1.000000000000000082E-05 ), #9365, 'distance_accuracy_value', 'NONE');
#10705=DIRECTION ( 'NONE',  ( 0.000000000000000000, -1.224646799147353207E-16, 1.000000000000000000 ) ) ;
#10709=LINE ( 'NONE', #218, #9128 ) ;
#10718=LINE ( 'NONE', #4752, #11716 ) ;
#10737=CARTESIAN_POINT ( 'NONE',  ( 4.200000000000001954, 0.000000000000000000, -2.200000000000018385 ) ) ;
#10742=ORIENTED_EDGE ( 'NONE', *, *, #4838, .F. ) ;
#10743=DIRECTION ( 'NONE',  ( -1.000000000000000000, 0.000000000000000000, 0.000000000000000000 ) ) ;
#10744=CIRCLE ( 'NONE', #10956, 1.535500000000000087 ) ;
#10769=VERTEX_POINT ( 'NONE', #2059 ) ;
#10784=DIRECTION ( 'NONE',  ( -1.000000000000000000, 0.000000000000000000, 0.000000000000000000 ) ) ;
#10802=ORIENTED_EDGE ( 'NONE', *, *, #481, .F. ) ;
#10805=EDGE_CURVE ( 'NONE', #4892, #6728, #2670, .T. ) ;
#10807=FACE_OUTER_BOUND ( 'NONE', #5008, .T. ) ;
#10823=EDGE_CURVE ( 'NONE', #12214, #1188, #2705, .T. ) ;
#10834=EDGE_CURVE ( 'NONE', #11320, #10019, #4965, .T. ) ;
#10836=VERTEX_POINT ( 'NONE', #7911 ) ;
#10840=FACE_OUTER_BOUND ( 'NONE', #6735, .T. ) ;
#10867=AXIS2_PLACEMENT_3D ( 'NONE', #9070, #251, #8103 ) ;
#10877=SURFACE_STYLE_USAGE ( .BOTH. , #6053 ) ;
#10892=EDGE_CURVE ( 'NONE', #10836, #3366, #11385, .T. ) ;
#10898=DIRECTION ( 'NONE',  ( 0.000000000000000000, 1.000000000000000000, 1.224646799147353207E-16 ) ) ;
#10902=DIRECTION ( 'NONE',  ( 0.000000000000000000, -0.4999999999999992784, 0.8660254037844389297 ) ) ;
#10922=EDGE_LOOP ( 'NONE', ( #3960, #8929, #2326, #3341 ) ) ;
#10924=ORIENTED_EDGE ( 'NONE', *, *, #6204, .F. ) ;
#10925=VECTOR ( 'NONE', #5675, 1000.000000000000000 ) ;
#10941=EDGE_LOOP ( 'NONE', ( #10924, #12308, #1887, #5980 ) ) ;
#10946=DIRECTION ( 'NONE',  ( -1.000000000000000000, 0.000000000000000000, 0.000000000000000000 ) ) ;
#10953=DIRECTION ( 'NONE',  ( -1.000000000000000000, 0.000000000000000000, 0.000000000000000000 ) ) ;
#10956=AXIS2_PLACEMENT_3D ( 'NONE', #10001, #11897, #9877 ) ;
#10961=PLANE ( 'NONE',  #1821 ) ;
#10967=EDGE_CURVE ( 'NONE', #5083, #11532, #9859, .T. ) ;
#10977=EDGE_CURVE ( 'NONE', #11940, #11433, #3689, .T. ) ;
#10986=DIRECTION ( 'NONE',  ( 0.000000000000000000, -1.000000000000000000, 0.000000000000000000 ) ) ;
#11008=LINE ( 'NONE', #5214, #8223 ) ;
#11014=DIRECTION ( 'NONE',  ( -1.000000000000000000, 0.000000000000000000, 0.000000000000000000 ) ) ;
#11062=VERTEX_POINT ( 'NONE', #7641 ) ;
#11102=AXIS2_PLACEMENT_3D ( 'NONE', #10622, #12448, #836 ) ;
#11124=EDGE_LOOP ( 'NONE', ( #2122, #5710, #3226 ) ) ;
#11137=ADVANCED_FACE ( 'NONE', ( #11694 ), #5829, .F. ) ;
#11150=AXIS2_PLACEMENT_3D ( 'NONE', #7673, #10684, #1746 ) ;
#11153=CARTESIAN_POINT ( 'NONE',  ( 0.1999999999999987899, 0.000000000000000000, 3.499999999999982681 ) ) ;
#11160=DIRECTION ( 'NONE',  ( -1.000000000000000000, 0.000000000000000000, 0.000000000000000000 ) ) ;
#11181=DIRECTION ( 'NONE',  ( -1.000000000000000000, 0.000000000000000000, 0.000000000000000000 ) ) ;
#11182=ORIENTED_EDGE ( 'NONE', *, *, #1282, .F. ) ;
#11185=CIRCLE ( 'NONE', #4394, 3.299999999999999822 ) ;
#11242=CARTESIAN_POINT ( 'NONE',  ( 34.00000000000000000, 0.000000000000000000, 1.609999999999982778 ) ) ;
#11278=DIRECTION ( 'NONE',  ( 0.000000000000000000, 0.000000000000000000, -1.000000000000000000 ) ) ;
#11298=DIRECTION ( 'NONE',  ( -1.000000000000000000, 0.000000000000000000, 0.000000000000000000 ) ) ;
#11302=ADVANCED_FACE ( 'NONE', ( #5305 ), #12275, .T. ) ;
#11320=VERTEX_POINT ( 'NONE', #2487 ) ;
#11326=CARTESIAN_POINT ( 'NONE',  ( 2.000000000000001776, 3.469446951953614189E-15, 1.535499999999998755 ) ) ;
#11358=CARTESIAN_POINT ( 'NONE',  ( 0.000000000000000000, 0.000000000000000000, 0.000000000000000000 ) ) ;
#11374=EDGE_CURVE ( 'NONE', #7142, #2431, #11618, .T. ) ;
#11385=LINE ( 'NONE', #3533, #3884 ) ;
#11386=ORIENTED_EDGE ( 'NONE', *, *, #12590, .F. ) ;
#11399=UNCERTAINTY_MEASURE_WITH_UNIT (LENGTH_MEASURE( 1.000000000000000082E-05 ), #255, 'distance_accuracy_value', 'NONE');
#11407=CARTESIAN_POINT ( 'NONE',  ( 0.1999999999999987899, 0.000000000000000000, -1.734723475976807094E-14 ) ) ;
#11433=VERTEX_POINT ( 'NONE', #917 ) ;
#11486=DIRECTION ( 'NONE',  ( 0.000000000000000000, 0.000000000000000000, 1.000000000000000000 ) ) ;
#11532=VERTEX_POINT ( 'NONE', #11746 ) ;
#11533=PLANE ( 'NONE',  #3161 ) ;
#11535=ORIENTED_EDGE ( 'NONE', *, *, #10892, .F. ) ;
#11540=CARTESIAN_POINT ( 'NONE',  ( 9.714451465470119729E-14, 0.8865213383406691516, -1.535500000000002085 ) ) ;
#11558=CARTESIAN_POINT ( 'NONE',  ( -31.74999999999995026, 0.000000000000000000, 3.499999999999982681 ) ) ;
#11600=FACE_OUTER_BOUND ( 'NONE', #6807, .T. ) ;
#11618=LINE ( 'NONE', #787, #4135 ) ;
#11627=DIRECTION ( 'NONE',  ( -1.000000000000000000, 0.000000000000000000, 0.000000000000000000 ) ) ;
#11658=ORIENTED_EDGE ( 'NONE', *, *, #2359, .F. ) ;
#11660=VECTOR ( 'NONE', #11627, 1000.000000000000000 ) ;
#11694=FACE_OUTER_BOUND ( 'NONE', #9249, .T. ) ;
#11716=VECTOR ( 'NONE', #10784, 1000.000000000000000 ) ;
#11746=CARTESIAN_POINT ( 'NONE',  ( 1.999999999999994893, 1.329782007511003838, -0.7677500000000010427 ) ) ;
#11751=DIRECTION ( 'NONE',  ( 0.000000000000000000, 0.000000000000000000, 1.000000000000000000 ) ) ;
#11768=CARTESIAN_POINT ( 'NONE',  ( 0.000000000000000000, -1.773042676681341856, 3.469446951953614189E-15 ) ) ;
#11770=EDGE_LOOP ( 'NONE', ( #5537, #2038, #7513 ) ) ;
#11808=CARTESIAN_POINT ( 'NONE',  ( 4.200000000000001954, 2.694222958124178486E-16, 2.199999999999983746 ) ) ;
#11815=DIRECTION ( 'NONE',  ( 0.000000000000000000, -8.560894001270036306E-16, -1.000000000000000000 ) ) ;
#11821=LINE ( 'NONE', #5759, #7101 ) ;
#11822=DIRECTION ( 'NONE',  ( 1.000000000000000000, 0.000000000000000000, 0.000000000000000000 ) ) ;
#11831=SHAPE_DEFINITION_REPRESENTATION ( #10056, #10094 ) ;
#11843=ADVANCED_FACE ( 'NONE', ( #8703 ), #6773, .T. ) ;
#11859=PLANE ( 'NONE',  #8473 ) ;
#11864=AXIS2_PLACEMENT_3D ( 'NONE', #12028, #3279, #2303 ) ;
#11897=DIRECTION ( 'NONE',  ( -1.000000000000000000, 0.000000000000000000, 0.000000000000000000 ) ) ;
#11940=VERTEX_POINT ( 'NONE', #2863 ) ;
#11946=DIRECTION ( 'NONE',  ( 0.000000000000000000, -0.5000000000000011102, -0.8660254037844379305 ) ) ;
#11951=CARTESIAN_POINT ( 'NONE',  ( 2.886521338340684917, 0.000000000000000000, 1.387778780781445676E-14 ) ) ;
#11958=MECHANICAL_DESIGN_GEOMETRIC_PRESENTATION_REPRESENTATION('',(#7628),#6190);
#11965=ADVANCED_FACE ( 'NONE', ( #9773 ), #11859, .T. ) ;
#11971=AXIS2_PLACEMENT_3D ( 'NONE', #7373, #11298, #3332 ) ;
#11981=ORIENTED_EDGE ( 'NONE', *, *, #5018, .T. ) ;
#11990=TOROIDAL_SURFACE ( 'NONE', #9094, 2.200000000000001066, 0.2000000000000000111 ) ;
#12005=LINE ( 'NONE', #1236, #5406 ) ;
#12028=CARTESIAN_POINT ( 'NONE',  ( 4.200000000000001954, 0.000000000000000000, -1.734723475976807094E-14 ) ) ;
#12054=EDGE_LOOP ( 'NONE', ( #6492, #6960, #8224, #393, #5256 ) ) ;
#12057=( NAMED_UNIT ( * ) SI_UNIT ( $, .STERADIAN. ) SOLID_ANGLE_UNIT ( ) );
#12066=MECHANICAL_DESIGN_GEOMETRIC_PRESENTATION_REPRESENTATION('',(#4240),#6717);
#12082=ORIENTED_EDGE ( 'NONE', *, *, #154, .F. ) ;
#12091=EDGE_CURVE ( 'NONE', #4994, #1632, #1091, .T. ) ;
#12135=AXIS2_PLACEMENT_3D ( 'NONE', #10003, #1134, #12696 ) ;
#12140=DIRECTION ( 'NONE',  ( 0.000000000000000000, -0.5000000000000012212, -0.8660254037844380415 ) ) ;
#12161=EDGE_CURVE ( 'NONE', #9207, #4167, #4583, .T. ) ;
#12170=EDGE_CURVE ( 'NONE', #1632, #9207, #1072, .T. ) ;
#12200=EDGE_CURVE ( 'NONE', #11320, #5702, #9492, .T. ) ;
#12206=CARTESIAN_POINT ( 'NONE',  ( 2.000000000000001776, 1.329782007511007169, 0.7677499999999976010 ) ) ;
#12214=VERTEX_POINT ( 'NONE', #381 ) ;
#12216=ORIENTED_EDGE ( 'NONE', *, *, #4455, .F. ) ;
#12233=FILL_AREA_STYLE_COLOUR ( '', #8355 ) ;
#12240=DIRECTION ( 'NONE',  ( -1.000000000000000000, 0.000000000000000000, 0.000000000000000000 ) ) ;
#12243=ORIENTED_EDGE ( 'NONE', *, *, #8008, .T. ) ;
#12267=DIRECTION ( 'NONE',  ( 0.000000000000000000, 0.000000000000000000, 1.000000000000000000 ) ) ;
#12275=CYLINDRICAL_SURFACE ( 'NONE', #11971, 2.000000000000000888 ) ;
#12287=CIRCLE ( 'NONE', #5274, 3.500000000000000000 ) ;
#12305=PRODUCT_DEFINITION_CONTEXT ( 'detailed design', #1067, 'design' ) ;
#12308=ORIENTED_EDGE ( 'NONE', *, *, #10823, .T. ) ;
#12342=ORIENTED_EDGE ( 'NONE', *, *, #481, .T. ) ;
#12351=EDGE_LOOP ( 'NONE', ( #10013, #3534, #4223, #5601, #4024 ) ) ;
#12363=ADVANCED_FACE ( 'NONE', ( #8685 ), #11533, .F. ) ;
#12390=AXIS2_PLACEMENT_3D ( 'NONE', #7287, #8308, #5348 ) ;
#12409=AXIS2_PLACEMENT_3D ( 'NONE', #10667, #4822, #8748 ) ;
#12411=DIRECTION ( 'NONE',  ( 0.000000000000000000, 0.000000000000000000, 1.000000000000000000 ) ) ;
#12422=AXIS2_PLACEMENT_3D ( 'NONE', #5707, #7392, #6428 ) ;
#12432=CARTESIAN_POINT ( 'NONE',  ( 2.000000000000001776, 0.000000000000000000, 0.000000000000000000 ) ) ;
#12433=ADVANCED_FACE ( 'NONE', ( #7964 ), #7845, .F. ) ;
#12446=LINE ( 'NONE', #9578, #10052 ) ;
#12448=DIRECTION ( 'NONE',  ( 1.000000000000000000, 0.000000000000000000, 0.000000000000000000 ) ) ;
#12469=DIRECTION ( 'NONE',  ( -0.7071067811865355823, 0.000000000000000000, 0.7071067811865595631 ) ) ;
#12480=EDGE_LOOP ( 'NONE', ( #5189, #7058, #2628, #6489 ) ) ;
#12491=CARTESIAN_POINT ( 'NONE',  ( 4.200000000000001954, 2.449293598294707893E-16, -2.000000000000018208 ) ) ;
#12505=LINE ( 'NONE', #11540, #2448 ) ;
#12536=CARTESIAN_POINT ( 'NONE',  ( 33.61000000000001364, 0.000000000000000000, 2.000000000000000888 ) ) ;
#12546=DIRECTION ( 'NONE',  ( 1.000000000000000000, 0.000000000000000000, 0.000000000000000000 ) ) ;
#12563=CONICAL_SURFACE ( 'NONE', #8435, 1.535500000000000087, 1.047197551196590748 ) ;
#12568=ORIENTED_EDGE ( 'NONE', *, *, #10977, .T. ) ;
#12590=EDGE_CURVE ( 'NONE', #2497, #2431, #9693, .T. ) ;
#12675=EDGE_LOOP ( 'NONE', ( #10363, #4900 ) ) ;
#12678=VERTEX_POINT ( 'NONE', #2313 ) ;
#12682=CARTESIAN_POINT ( 'NONE',  ( 4.000000000000003553, 0.000000000000000000, 0.000000000000000000 ) ) ;
#12685=FACE_BOUND ( 'NONE', #2344, .T. ) ;
#12696=DIRECTION ( 'NONE',  ( 0.000000000000000000, 0.000000000000000000, 1.000000000000000000 ) ) ;
#12729=CARTESIAN_POINT ( 'NONE',  ( 2.000000000000001776, 1.773042676681341856, -3.469446951953614189E-15 ) ) ;
#12732=EDGE_CURVE ( 'NONE', #8146, #2957, #5816, .T. ) ;
#12736=AXIS2_PLACEMENT_3D ( 'NONE', #4754, #9497, #9559 ) ;
#12745=ORIENTED_EDGE ( 'NONE', *, *, #9372, .T. ) ;
ENDSEC;
END-ISO-10303-21;
